ISO-10303-21;
HEADER;
/* Generated by software containing ST-Developer
 * from STEP Tools, Inc. (www.steptools.com) 
 */

FILE_DESCRIPTION(
/* description */ ('Hook toggle clamp'),
/* implementation_level */ '2;1');

FILE_NAME(
/* name */ 'Ground pivot screw.step',
/* time_stamp */ '2026-10-27T21:56:56-07:00',
/* author */ (''),
/* organization */ (''),
/* preprocessor_version */ 'ST-DEVELOPER v20.2',
/* originating_system */ 'Autodesk Translation Framework v15.17.0.0',
/* authorisation */ '');

FILE_SCHEMA (('AUTOMOTIVE_DESIGN { 1 0 10303 214 3 1 1 }'));
ENDSEC;

DATA;
#10=MECHANICAL_DESIGN_GEOMETRIC_PRESENTATION_REPRESENTATION('',(#190),#5458);
#129=(
BOUNDED_CURVE()
B_SPLINE_CURVE(2,(#4591,#4592,#4593),.UNSPECIFIED.,.F.,.F.)
B_SPLINE_CURVE_WITH_KNOTS((3,3),(0.144988513094728,0.791574906712449),
 .UNSPECIFIED.)
CURVE()
GEOMETRIC_REPRESENTATION_ITEM()
RATIONAL_B_SPLINE_CURVE((1.09282032302755,1.26188021535082,1.09282032302931))
REPRESENTATION_ITEM('')
);
#130=(
BOUNDED_CURVE()
B_SPLINE_CURVE(2,(#4595,#4596,#4597),.UNSPECIFIED.,.F.,.F.)
B_SPLINE_CURVE_WITH_KNOTS((3,3),(0.144988513094728,0.791574906712449),
 .UNSPECIFIED.)
CURVE()
GEOMETRIC_REPRESENTATION_ITEM()
RATIONAL_B_SPLINE_CURVE((1.09282032302755,1.26188021535082,1.09282032302931))
REPRESENTATION_ITEM('')
);
#131=(
BOUNDED_CURVE()
B_SPLINE_CURVE(2,(#4599,#4600,#4601),.UNSPECIFIED.,.F.,.F.)
B_SPLINE_CURVE_WITH_KNOTS((3,3),(0.144988513094728,0.791574906712449),
 .UNSPECIFIED.)
CURVE()
GEOMETRIC_REPRESENTATION_ITEM()
RATIONAL_B_SPLINE_CURVE((1.09282032302755,1.26188021535082,1.09282032302931))
REPRESENTATION_ITEM('')
);
#132=(
BOUNDED_CURVE()
B_SPLINE_CURVE(2,(#4603,#4604,#4605),.UNSPECIFIED.,.F.,.F.)
B_SPLINE_CURVE_WITH_KNOTS((3,3),(0.144988513094728,0.791574906712449),
 .UNSPECIFIED.)
CURVE()
GEOMETRIC_REPRESENTATION_ITEM()
RATIONAL_B_SPLINE_CURVE((1.09282032302755,1.26188021535082,1.09282032302931))
REPRESENTATION_ITEM('')
);
#133=(
BOUNDED_CURVE()
B_SPLINE_CURVE(2,(#4607,#4608,#4609),.UNSPECIFIED.,.F.,.F.)
B_SPLINE_CURVE_WITH_KNOTS((3,3),(0.144988513094728,0.791574906712449),
 .UNSPECIFIED.)
CURVE()
GEOMETRIC_REPRESENTATION_ITEM()
RATIONAL_B_SPLINE_CURVE((1.09282032302755,1.26188021535082,1.09282032302931))
REPRESENTATION_ITEM('')
);
#134=(
BOUNDED_CURVE()
B_SPLINE_CURVE(2,(#4610,#4611,#4612),.UNSPECIFIED.,.F.,.F.)
B_SPLINE_CURVE_WITH_KNOTS((3,3),(0.144988513094727,0.791574906712449),
 .UNSPECIFIED.)
CURVE()
GEOMETRIC_REPRESENTATION_ITEM()
RATIONAL_B_SPLINE_CURVE((1.09282032302755,1.26188021535082,1.09282032302931))
REPRESENTATION_ITEM('')
);
#147=CONICAL_SURFACE('',#3227,0.576175134594813,1.0471975511966);
#156=SHAPE_REPRESENTATION_RELATIONSHIP('SRR','None',#5537,#173);
#173=ADVANCED_BREP_SHAPE_REPRESENTATION('',(#207),#5439);
#190=STYLED_ITEM('',(#5724),#207);
#207=MANIFOLD_SOLID_BREP('Body1',#2971);
#236=FACE_BOUND('',#622,.T.);
#303=PLANE('',#3223);
#304=PLANE('',#3229);
#305=PLANE('',#3230);
#306=PLANE('',#3231);
#307=PLANE('',#3232);
#308=PLANE('',#3233);
#309=PLANE('',#3234);
#310=PLANE('',#3235);
#311=PLANE('',#3236);
#424=FACE_OUTER_BOUND('',#611,.T.);
#425=FACE_OUTER_BOUND('',#612,.T.);
#426=FACE_OUTER_BOUND('',#613,.T.);
#427=FACE_OUTER_BOUND('',#614,.T.);
#428=FACE_OUTER_BOUND('',#615,.T.);
#429=FACE_OUTER_BOUND('',#616,.T.);
#430=FACE_OUTER_BOUND('',#617,.T.);
#431=FACE_OUTER_BOUND('',#618,.T.);
#432=FACE_OUTER_BOUND('',#619,.T.);
#433=FACE_OUTER_BOUND('',#620,.T.);
#434=FACE_OUTER_BOUND('',#621,.T.);
#611=EDGE_LOOP('',(#2151));
#612=EDGE_LOOP('',(#2152,#2153,#2154,#2155));
#613=EDGE_LOOP('',(#2156,#2157,#2158,#2159,#2160,#2161,#2162,#2163,#2164));
#614=EDGE_LOOP('',(#2165,#2166,#2167,#2168));
#615=EDGE_LOOP('',(#2169,#2170,#2171,#2172));
#616=EDGE_LOOP('',(#2173,#2174,#2175,#2176));
#617=EDGE_LOOP('',(#2177,#2178,#2179,#2180));
#618=EDGE_LOOP('',(#2181,#2182,#2183,#2184));
#619=EDGE_LOOP('',(#2185,#2186,#2187,#2188));
#620=EDGE_LOOP('',(#2189));
#621=EDGE_LOOP('',(#2190,#2191,#2192,#2193,#2194,#2195));
#622=EDGE_LOOP('',(#2196));
#858=LINE('',#4583,#1095);
#859=LINE('',#4589,#1096);
#860=LINE('',#4615,#1097);
#861=LINE('',#4617,#1098);
#862=LINE('',#4618,#1099);
#863=LINE('',#4621,#1100);
#864=LINE('',#4622,#1101);
#865=LINE('',#4625,#1102);
#866=LINE('',#4626,#1103);
#867=LINE('',#4629,#1104);
#868=LINE('',#4630,#1105);
#869=LINE('',#4633,#1106);
#870=LINE('',#4634,#1107);
#871=LINE('',#4636,#1108);
#1095=VECTOR('',#3674,0.3);
#1096=VECTOR('',#3681,0.576175134594813);
#1097=VECTOR('',#3684,1.);
#1098=VECTOR('',#3685,1.);
#1099=VECTOR('',#3686,1.);
#1100=VECTOR('',#3689,1.);
#1101=VECTOR('',#3690,1.);
#1102=VECTOR('',#3693,1.);
#1103=VECTOR('',#3694,1.);
#1104=VECTOR('',#3697,1.);
#1105=VECTOR('',#3698,1.);
#1106=VECTOR('',#3701,1.);
#1107=VECTOR('',#3702,1.);
#1108=VECTOR('',#3705,1.);
#1281=CIRCLE('',#3224,0.2942);
#1282=CIRCLE('',#3226,0.2942);
#1283=CIRCLE('',#3228,0.475);
#1432=VERTEX_POINT('',#4579);
#1433=VERTEX_POINT('',#4582);
#1434=VERTEX_POINT('',#4586);
#1435=VERTEX_POINT('',#4588);
#1436=VERTEX_POINT('',#4590);
#1437=VERTEX_POINT('',#4594);
#1438=VERTEX_POINT('',#4598);
#1439=VERTEX_POINT('',#4602);
#1440=VERTEX_POINT('',#4606);
#1441=VERTEX_POINT('',#4614);
#1442=VERTEX_POINT('',#4616);
#1443=VERTEX_POINT('',#4620);
#1444=VERTEX_POINT('',#4624);
#1445=VERTEX_POINT('',#4628);
#1446=VERTEX_POINT('',#4632);
#1702=EDGE_CURVE('',#1432,#1432,#1281,.T.);
#1703=EDGE_CURVE('',#1432,#1433,#858,.T.);
#1704=EDGE_CURVE('',#1433,#1433,#1282,.F.);
#1705=EDGE_CURVE('',#1434,#1434,#1283,.T.);
#1706=EDGE_CURVE('',#1434,#1435,#859,.T.);
#1707=EDGE_CURVE('',#1436,#1435,#129,.T.);
#1708=EDGE_CURVE('',#1437,#1436,#130,.T.);
#1709=EDGE_CURVE('',#1438,#1437,#131,.T.);
#1710=EDGE_CURVE('',#1439,#1438,#132,.T.);
#1711=EDGE_CURVE('',#1440,#1439,#133,.T.);
#1712=EDGE_CURVE('',#1435,#1440,#134,.T.);
#1713=EDGE_CURVE('',#1441,#1439,#860,.T.);
#1714=EDGE_CURVE('',#1441,#1442,#861,.T.);
#1715=EDGE_CURVE('',#1442,#1440,#862,.T.);
#1716=EDGE_CURVE('',#1443,#1438,#863,.T.);
#1717=EDGE_CURVE('',#1443,#1441,#864,.T.);
#1718=EDGE_CURVE('',#1444,#1437,#865,.T.);
#1719=EDGE_CURVE('',#1444,#1443,#866,.T.);
#1720=EDGE_CURVE('',#1445,#1436,#867,.T.);
#1721=EDGE_CURVE('',#1445,#1444,#868,.T.);
#1722=EDGE_CURVE('',#1446,#1435,#869,.T.);
#1723=EDGE_CURVE('',#1446,#1445,#870,.T.);
#1724=EDGE_CURVE('',#1442,#1446,#871,.T.);
#2151=ORIENTED_EDGE('',*,*,#1702,.F.);
#2152=ORIENTED_EDGE('',*,*,#1702,.T.);
#2153=ORIENTED_EDGE('',*,*,#1703,.T.);
#2154=ORIENTED_EDGE('',*,*,#1704,.F.);
#2155=ORIENTED_EDGE('',*,*,#1703,.F.);
#2156=ORIENTED_EDGE('',*,*,#1705,.F.);
#2157=ORIENTED_EDGE('',*,*,#1706,.T.);
#2158=ORIENTED_EDGE('',*,*,#1707,.F.);
#2159=ORIENTED_EDGE('',*,*,#1708,.F.);
#2160=ORIENTED_EDGE('',*,*,#1709,.F.);
#2161=ORIENTED_EDGE('',*,*,#1710,.F.);
#2162=ORIENTED_EDGE('',*,*,#1711,.F.);
#2163=ORIENTED_EDGE('',*,*,#1712,.F.);
#2164=ORIENTED_EDGE('',*,*,#1706,.F.);
#2165=ORIENTED_EDGE('',*,*,#1711,.T.);
#2166=ORIENTED_EDGE('',*,*,#1713,.F.);
#2167=ORIENTED_EDGE('',*,*,#1714,.T.);
#2168=ORIENTED_EDGE('',*,*,#1715,.T.);
#2169=ORIENTED_EDGE('',*,*,#1710,.T.);
#2170=ORIENTED_EDGE('',*,*,#1716,.F.);
#2171=ORIENTED_EDGE('',*,*,#1717,.T.);
#2172=ORIENTED_EDGE('',*,*,#1713,.T.);
#2173=ORIENTED_EDGE('',*,*,#1709,.T.);
#2174=ORIENTED_EDGE('',*,*,#1718,.F.);
#2175=ORIENTED_EDGE('',*,*,#1719,.T.);
#2176=ORIENTED_EDGE('',*,*,#1716,.T.);
#2177=ORIENTED_EDGE('',*,*,#1708,.T.);
#2178=ORIENTED_EDGE('',*,*,#1720,.F.);
#2179=ORIENTED_EDGE('',*,*,#1721,.T.);
#2180=ORIENTED_EDGE('',*,*,#1718,.T.);
#2181=ORIENTED_EDGE('',*,*,#1707,.T.);
#2182=ORIENTED_EDGE('',*,*,#1722,.F.);
#2183=ORIENTED_EDGE('',*,*,#1723,.T.);
#2184=ORIENTED_EDGE('',*,*,#1720,.T.);
#2185=ORIENTED_EDGE('',*,*,#1712,.T.);
#2186=ORIENTED_EDGE('',*,*,#1715,.F.);
#2187=ORIENTED_EDGE('',*,*,#1724,.T.);
#2188=ORIENTED_EDGE('',*,*,#1722,.T.);
#2189=ORIENTED_EDGE('',*,*,#1705,.T.);
#2190=ORIENTED_EDGE('',*,*,#1719,.F.);
#2191=ORIENTED_EDGE('',*,*,#1721,.F.);
#2192=ORIENTED_EDGE('',*,*,#1723,.F.);
#2193=ORIENTED_EDGE('',*,*,#1724,.F.);
#2194=ORIENTED_EDGE('',*,*,#1714,.F.);
#2195=ORIENTED_EDGE('',*,*,#1717,.F.);
#2196=ORIENTED_EDGE('',*,*,#1704,.T.);
#2755=CYLINDRICAL_SURFACE('',#3225,0.2942);
#2828=ADVANCED_FACE('',(#424),#303,.F.);
#2829=ADVANCED_FACE('',(#425),#2755,.T.);
#2830=ADVANCED_FACE('',(#426),#147,.T.);
#2831=ADVANCED_FACE('',(#427),#304,.T.);
#2832=ADVANCED_FACE('',(#428),#305,.T.);
#2833=ADVANCED_FACE('',(#429),#306,.T.);
#2834=ADVANCED_FACE('',(#430),#307,.T.);
#2835=ADVANCED_FACE('',(#431),#308,.T.);
#2836=ADVANCED_FACE('',(#432),#309,.T.);
#2837=ADVANCED_FACE('',(#433),#310,.T.);
#2838=ADVANCED_FACE('',(#434,#236),#311,.F.);
#2971=CLOSED_SHELL('',(#2828,#2829,#2830,#2831,#2832,#2833,#2834,#2835,
#2836,#2837,#2838));
#3222=AXIS2_PLACEMENT_3D('',#4577,#3666,#3667);
#3223=AXIS2_PLACEMENT_3D('',#4578,#3668,#3669);
#3224=AXIS2_PLACEMENT_3D('',#4580,#3670,#3671);
#3225=AXIS2_PLACEMENT_3D('',#4581,#3672,#3673);
#3226=AXIS2_PLACEMENT_3D('',#4584,#3675,#3676);
#3227=AXIS2_PLACEMENT_3D('',#4585,#3677,#3678);
#3228=AXIS2_PLACEMENT_3D('',#4587,#3679,#3680);
#3229=AXIS2_PLACEMENT_3D('',#4613,#3682,#3683);
#3230=AXIS2_PLACEMENT_3D('',#4619,#3687,#3688);
#3231=AXIS2_PLACEMENT_3D('',#4623,#3691,#3692);
#3232=AXIS2_PLACEMENT_3D('',#4627,#3695,#3696);
#3233=AXIS2_PLACEMENT_3D('',#4631,#3699,#3700);
#3234=AXIS2_PLACEMENT_3D('',#4635,#3703,#3704);
#3235=AXIS2_PLACEMENT_3D('',#4637,#3706,#3707);
#3236=AXIS2_PLACEMENT_3D('',#4638,#3708,#3709);
#3666=DIRECTION('axis',(0.,0.,1.));
#3667=DIRECTION('refdir',(1.,0.,0.));
#3668=DIRECTION('center_axis',(0.,1.,0.));
#3669=DIRECTION('ref_axis',(0.,0.,1.));
#3670=DIRECTION('center_axis',(0.,1.,0.));
#3671=DIRECTION('ref_axis',(1.,0.,0.));
#3672=DIRECTION('center_axis',(0.,-1.,0.));
#3673=DIRECTION('ref_axis',(1.,0.,0.));
#3674=DIRECTION('',(0.,1.,0.));
#3675=DIRECTION('center_axis',(0.,-1.,0.));
#3676=DIRECTION('ref_axis',(1.,0.,0.));
#3677=DIRECTION('center_axis',(0.,-1.,0.));
#3678=DIRECTION('ref_axis',(1.,0.,0.));
#3679=DIRECTION('center_axis',(0.,1.,0.));
#3680=DIRECTION('ref_axis',(1.,0.,0.));
#3681=DIRECTION('',(-0.866025403784439,-0.5,-1.06057523872491E-16));
#3682=DIRECTION('center_axis',(1.92296268638356E-16,0.,-1.));
#3683=DIRECTION('ref_axis',(-1.,0.,-1.92296268638356E-16));
#3684=DIRECTION('',(0.,1.,0.));
#3685=DIRECTION('',(-1.,0.,-1.92296268638356E-16));
#3686=DIRECTION('',(0.,1.,0.));
#3687=DIRECTION('center_axis',(0.866025403784439,0.,-0.5));
#3688=DIRECTION('ref_axis',(-0.5,0.,-0.866025403784439));
#3689=DIRECTION('',(0.,1.,0.));
#3690=DIRECTION('',(-0.5,0.,-0.866025403784439));
#3691=DIRECTION('center_axis',(0.866025403784439,0.,0.5));
#3692=DIRECTION('ref_axis',(0.5,0.,-0.866025403784439));
#3693=DIRECTION('',(0.,1.,0.));
#3694=DIRECTION('',(0.5,0.,-0.866025403784439));
#3695=DIRECTION('center_axis',(-1.92296268638356E-16,0.,1.));
#3696=DIRECTION('ref_axis',(1.,0.,1.92296268638356E-16));
#3697=DIRECTION('',(0.,1.,0.));
#3698=DIRECTION('',(1.,0.,1.92296268638356E-16));
#3699=DIRECTION('center_axis',(-0.866025403784439,0.,0.5));
#3700=DIRECTION('ref_axis',(0.5,0.,0.866025403784439));
#3701=DIRECTION('',(0.,1.,0.));
#3702=DIRECTION('',(0.5,0.,0.866025403784439));
#3703=DIRECTION('center_axis',(-0.866025403784439,0.,-0.5));
#3704=DIRECTION('ref_axis',(-0.5,0.,0.866025403784439));
#3705=DIRECTION('',(-0.5,0.,0.866025403784438));
#3706=DIRECTION('center_axis',(0.,1.,0.));
#3707=DIRECTION('ref_axis',(0.,0.,1.));
#3708=DIRECTION('center_axis',(0.,1.,0.));
#3709=DIRECTION('ref_axis',(1.,0.,0.));
#4577=CARTESIAN_POINT('',(0.,0.,0.));
#4578=CARTESIAN_POINT('Origin',(0.,-2.,0.));
#4579=CARTESIAN_POINT('',(-0.2942,-2.,3.60291088309151E-17));
#4580=CARTESIAN_POINT('Origin',(0.,-2.,0.));
#4581=CARTESIAN_POINT('Origin',(0.,-1.445,0.));
#4582=CARTESIAN_POINT('',(-0.2942,0.,-3.60291088309151E-17));
#4583=CARTESIAN_POINT('',(-0.2942,-1.445,-3.60291088309151E-17));
#4584=CARTESIAN_POINT('Origin',(0.,0.,0.));
#4585=CARTESIAN_POINT('Origin',(0.,0.341586508806388,0.));
#4586=CARTESIAN_POINT('',(-0.475,0.4,-5.81707229594993E-17));
#4587=CARTESIAN_POINT('Origin',(0.,0.4,0.));
#4588=CARTESIAN_POINT('',(-0.577350269189626,0.340908044531739,-7.07050159149938E-17));
#4589=CARTESIAN_POINT('',(-0.576175134594813,0.341586508806388,-7.05611034329833E-17));
#4590=CARTESIAN_POINT('',(-0.288675134594813,0.340908044531739,0.5));
#4591=CARTESIAN_POINT('Ctrl Pts',(-0.288675134594813,0.340908044531739,
0.5));
#4592=CARTESIAN_POINT('Ctrl Pts',(-0.433012701893303,0.424241377863696,
0.249999999998124));
#4593=CARTESIAN_POINT('Ctrl Pts',(-0.577350269189626,0.340908044531739,
-7.07050159149938E-17));
#4594=CARTESIAN_POINT('',(0.288675134594813,0.340908044531739,0.5));
#4595=CARTESIAN_POINT('Ctrl Pts',(0.288675134594813,0.340908044531739,0.5));
#4596=CARTESIAN_POINT('Ctrl Pts',(-2.16648921025353E-12,0.424241377863696,
0.5));
#4597=CARTESIAN_POINT('Ctrl Pts',(-0.288675134594813,0.340908044531739,
0.5));
#4598=CARTESIAN_POINT('',(0.577350269189626,0.340908044531739,0.));
#4599=CARTESIAN_POINT('Ctrl Pts',(0.577350269189626,0.340908044531739,0.));
#4600=CARTESIAN_POINT('Ctrl Pts',(0.433012701891136,0.424241377863697,0.250000000001876));
#4601=CARTESIAN_POINT('Ctrl Pts',(0.288675134594813,0.340908044531739,0.5));
#4602=CARTESIAN_POINT('',(0.288675134594813,0.340908044531739,-0.5));
#4603=CARTESIAN_POINT('Ctrl Pts',(0.288675134594813,0.340908044531739,-0.5));
#4604=CARTESIAN_POINT('Ctrl Pts',(0.433012701893303,0.424241377863696,-0.249999999998124));
#4605=CARTESIAN_POINT('Ctrl Pts',(0.577350269189626,0.340908044531739,0.));
#4606=CARTESIAN_POINT('',(-0.288675134594813,0.340908044531739,-0.5));
#4607=CARTESIAN_POINT('Ctrl Pts',(-0.288675134594813,0.340908044531739,
-0.5));
#4608=CARTESIAN_POINT('Ctrl Pts',(2.16660023255599E-12,0.424241377863696,
-0.5));
#4609=CARTESIAN_POINT('Ctrl Pts',(0.288675134594813,0.340908044531739,-0.5));
#4610=CARTESIAN_POINT('Ctrl Pts',(-0.577350269189626,0.340908044531739,
-7.07050159149938E-17));
#4611=CARTESIAN_POINT('Ctrl Pts',(-0.433012701891136,0.424241377863697,
-0.250000000001876));
#4612=CARTESIAN_POINT('Ctrl Pts',(-0.288675134594813,0.340908044531739,
-0.5));
#4613=CARTESIAN_POINT('Origin',(0.288675134594813,0.,-0.5));
#4614=CARTESIAN_POINT('',(0.288675134594813,0.,-0.5));
#4615=CARTESIAN_POINT('',(0.288675134594813,0.,-0.5));
#4616=CARTESIAN_POINT('',(-0.288675134594813,0.,-0.5));
#4617=CARTESIAN_POINT('',(0.288675134594813,0.,-0.5));
#4618=CARTESIAN_POINT('',(-0.288675134594813,0.,-0.5));
#4619=CARTESIAN_POINT('Origin',(0.577350269189626,0.,0.));
#4620=CARTESIAN_POINT('',(0.577350269189626,0.,0.));
#4621=CARTESIAN_POINT('',(0.577350269189626,0.,0.));
#4622=CARTESIAN_POINT('',(0.577350269189626,0.,0.));
#4623=CARTESIAN_POINT('Origin',(0.288675134594813,0.,0.5));
#4624=CARTESIAN_POINT('',(0.288675134594813,0.,0.5));
#4625=CARTESIAN_POINT('',(0.288675134594813,0.,0.5));
#4626=CARTESIAN_POINT('',(0.288675134594813,0.,0.5));
#4627=CARTESIAN_POINT('Origin',(-0.288675134594813,0.,0.5));
#4628=CARTESIAN_POINT('',(-0.288675134594813,0.,0.5));
#4629=CARTESIAN_POINT('',(-0.288675134594813,0.,0.5));
#4630=CARTESIAN_POINT('',(-0.288675134594813,0.,0.5));
#4631=CARTESIAN_POINT('Origin',(-0.577350269189626,0.,-7.07050159149938E-17));
#4632=CARTESIAN_POINT('',(-0.577350269189626,0.,-7.07050159149938E-17));
#4633=CARTESIAN_POINT('',(-0.577350269189626,0.,-7.07050159149938E-17));
#4634=CARTESIAN_POINT('',(-0.577350269189626,0.,-7.07050159149938E-17));
#4635=CARTESIAN_POINT('Origin',(-0.288675134594813,0.,-0.5));
#4636=CARTESIAN_POINT('',(-0.288675134594813,0.,-0.5));
#4637=CARTESIAN_POINT('Origin',(0.,0.4,0.));
#4638=CARTESIAN_POINT('Origin',(0.,0.,0.));
#5416=UNCERTAINTY_MEASURE_WITH_UNIT(LENGTH_MEASURE(0.001),#5459,
'DISTANCE_ACCURACY_VALUE',
'Maximum model space distance between geometric entities at asserted c
onnectivities');
#5435=UNCERTAINTY_MEASURE_WITH_UNIT(LENGTH_MEASURE(0.001),#5459,
'DISTANCE_ACCURACY_VALUE',
'Maximum model space distance between geometric entities at asserted c
onnectivities');
#5439=(
GEOMETRIC_REPRESENTATION_CONTEXT(3)
GLOBAL_UNCERTAINTY_ASSIGNED_CONTEXT((#5416))
GLOBAL_UNIT_ASSIGNED_CONTEXT((#5459,#5461,#5462))
REPRESENTATION_CONTEXT('','3D')
);
#5458=(
GEOMETRIC_REPRESENTATION_CONTEXT(3)
GLOBAL_UNCERTAINTY_ASSIGNED_CONTEXT((#5435))
GLOBAL_UNIT_ASSIGNED_CONTEXT((#5459,#5461,#5462))
REPRESENTATION_CONTEXT('','3D')
);
#5459=(
LENGTH_UNIT()
NAMED_UNIT(*)
SI_UNIT(.CENTI.,.METRE.)
);
#5461=(
NAMED_UNIT(*)
PLANE_ANGLE_UNIT()
SI_UNIT($,.RADIAN.)
);
#5462=(
NAMED_UNIT(*)
SI_UNIT($,.STERADIAN.)
SOLID_ANGLE_UNIT()
);
#5466=SHAPE_DEFINITION_REPRESENTATION(#5488,#5537);
#5488=PRODUCT_DEFINITION_SHAPE('',$,#5560);
#5537=SHAPE_REPRESENTATION('',(#3222),#5439);
#5556=PRODUCT_DEFINITION_CONTEXT('part definition',#5624,'design');
#5560=PRODUCT_DEFINITION('Ground pivot screw','Ground pivot screw',#5582,
#5556);
#5582=PRODUCT_DEFINITION_FORMATION('',$,#5629);
#5624=APPLICATION_CONTEXT(
'Core Data for Automotive Mechanical Design Process');
#5625=PRODUCT_CONTEXT('part definition',#5624,'mechanical');
#5629=PRODUCT('Ground pivot screw','Ground pivot screw',
'Ground pivot screw',(#5625));
#5718=COLOUR_RGB('Black',0.12,0.14,0.17);
#5719=FILL_AREA_STYLE_COLOUR('',#5718);
#5720=FILL_AREA_STYLE('',(#5719));
#5721=SURFACE_STYLE_FILL_AREA(#5720);
#5722=SURFACE_SIDE_STYLE('',(#5721));
#5723=SURFACE_STYLE_USAGE(.BOTH.,#5722);
#5724=PRESENTATION_STYLE_ASSIGNMENT((#5723));
ENDSEC;
END-ISO-10303-21;
